ISO-10303-21;
HEADER;
/* Generated by software containing ST-Developer
 * from STEP Tools, Inc. (www.steptools.com) 
 */

FILE_DESCRIPTION(
/* description */ ('Guided pneumatic stop gate'),
/* implementation_level */ '2;1');

FILE_NAME(
/* name */ 'Cap Screw - M4x16.step',
/* time_stamp */ '2026-10-27T21:43:45-07:00',
/* author */ (''),
/* organization */ (''),
/* preprocessor_version */ 'ST-DEVELOPER v20.2',
/* originating_system */ 'Autodesk Translation Framework v15.17.0.0',
/* authorisation */ '');

FILE_SCHEMA (('AUTOMOTIVE_DESIGN { 1 0 10303 214 3 1 1 }'));
ENDSEC;

DATA;
#10=MECHANICAL_DESIGN_GEOMETRIC_PRESENTATION_REPRESENTATION('',(#566),#14392);
#418=ORIENTED_CLOSED_SHELL('',*,#7910,.F.);
#422=BREP_WITH_VOIDS('Body1',#7909,(#418));
#441=CONICAL_SURFACE('',#9193,0.325,0.785398163397448);
#442=CONICAL_SURFACE('',#9197,0.335,0.785398163397448);
#443=CONICAL_SURFACE('',#9201,0.21,0.463647609000806);
#444=CONICAL_SURFACE('',#9205,0.18,0.785398163397448);
#482=SHAPE_REPRESENTATION_RELATIONSHIP('SRR','None',#14619,#524);
#524=ADVANCED_BREP_SHAPE_REPRESENTATION('',(#422),#14381);
#566=STYLED_ITEM('',(#14898),#422);
#797=FACE_BOUND('',#2154,.T.);
#1051=PLANE('',#9191);
#1052=PLANE('',#9199);
#1053=PLANE('',#9207);
#1054=PLANE('',#9208);
#1055=PLANE('',#9209);
#1056=PLANE('',#9210);
#1057=PLANE('',#9211);
#1058=PLANE('',#9212);
#1059=PLANE('',#9213);
#1060=PLANE('',#9214);
#1061=PLANE('',#9215);
#1492=FACE_OUTER_BOUND('',#2149,.T.);
#1493=FACE_OUTER_BOUND('',#2150,.T.);
#1494=FACE_OUTER_BOUND('',#2151,.T.);
#1495=FACE_OUTER_BOUND('',#2152,.T.);
#1496=FACE_OUTER_BOUND('',#2153,.T.);
#1497=FACE_OUTER_BOUND('',#2155,.T.);
#1498=FACE_OUTER_BOUND('',#2156,.T.);
#1499=FACE_OUTER_BOUND('',#2157,.T.);
#1500=FACE_OUTER_BOUND('',#2158,.T.);
#1501=FACE_OUTER_BOUND('',#2159,.T.);
#1502=FACE_OUTER_BOUND('',#2160,.T.);
#1503=FACE_OUTER_BOUND('',#2161,.T.);
#1504=FACE_OUTER_BOUND('',#2162,.T.);
#1505=FACE_OUTER_BOUND('',#2163,.T.);
#1506=FACE_OUTER_BOUND('',#2164,.T.);
#1507=FACE_OUTER_BOUND('',#2165,.T.);
#1508=FACE_OUTER_BOUND('',#2166,.T.);
#2149=EDGE_LOOP('',(#6818));
#2150=EDGE_LOOP('',(#6819,#6820,#6821,#6822));
#2151=EDGE_LOOP('',(#6823,#6824,#6825,#6826));
#2152=EDGE_LOOP('',(#6827,#6828,#6829,#6830));
#2153=EDGE_LOOP('',(#6831));
#2154=EDGE_LOOP('',(#6832));
#2155=EDGE_LOOP('',(#6833,#6834,#6835,#6836));
#2156=EDGE_LOOP('',(#6837,#6838,#6839,#6840));
#2157=EDGE_LOOP('',(#6841,#6842,#6843,#6844));
#2158=EDGE_LOOP('',(#6845));
#2159=EDGE_LOOP('',(#6846,#6847,#6848,#6849));
#2160=EDGE_LOOP('',(#6850,#6851,#6852,#6853));
#2161=EDGE_LOOP('',(#6854,#6855,#6856,#6857));
#2162=EDGE_LOOP('',(#6858,#6859,#6860,#6861));
#2163=EDGE_LOOP('',(#6862,#6863,#6864,#6865));
#2164=EDGE_LOOP('',(#6866,#6867,#6868,#6869));
#2165=EDGE_LOOP('',(#6870,#6871,#6872,#6873,#6874,#6875));
#2166=EDGE_LOOP('',(#6876,#6877,#6878,#6879,#6880,#6881));
#2693=LINE('',#13667,#3238);
#2694=LINE('',#13671,#3239);
#2695=LINE('',#13675,#3240);
#2696=LINE('',#13682,#3241);
#2697=LINE('',#13686,#3242);
#2698=LINE('',#13690,#3243);
#2699=LINE('',#13695,#3244);
#2700=LINE('',#13697,#3245);
#2701=LINE('',#13699,#3246);
#2702=LINE('',#13700,#3247);
#2703=LINE('',#13703,#3248);
#2704=LINE('',#13705,#3249);
#2705=LINE('',#13706,#3250);
#2706=LINE('',#13709,#3251);
#2707=LINE('',#13711,#3252);
#2708=LINE('',#13712,#3253);
#2709=LINE('',#13715,#3254);
#2710=LINE('',#13717,#3255);
#2711=LINE('',#13718,#3256);
#2712=LINE('',#13721,#3257);
#2713=LINE('',#13723,#3258);
#2714=LINE('',#13724,#3259);
#2715=LINE('',#13726,#3260);
#2716=LINE('',#13727,#3261);
#3238=VECTOR('',#11418,0.325);
#3239=VECTOR('',#11423,0.35);
#3240=VECTOR('',#11428,0.335);
#3241=VECTOR('',#11437,0.21);
#3242=VECTOR('',#11442,0.2);
#3243=VECTOR('',#11447,0.18);
#3244=VECTOR('',#11452,1.);
#3245=VECTOR('',#11453,1.);
#3246=VECTOR('',#11454,1.);
#3247=VECTOR('',#11455,1.);
#3248=VECTOR('',#11458,1.);
#3249=VECTOR('',#11459,1.);
#3250=VECTOR('',#11460,1.);
#3251=VECTOR('',#11463,1.);
#3252=VECTOR('',#11464,1.);
#3253=VECTOR('',#11465,1.);
#3254=VECTOR('',#11468,1.);
#3255=VECTOR('',#11469,1.);
#3256=VECTOR('',#11470,1.);
#3257=VECTOR('',#11473,1.);
#3258=VECTOR('',#11474,1.);
#3259=VECTOR('',#11475,1.);
#3260=VECTOR('',#11478,1.);
#3261=VECTOR('',#11479,1.);
#3678=CIRCLE('',#9192,0.3);
#3679=CIRCLE('',#9194,0.35);
#3680=CIRCLE('',#9196,0.35);
#3681=CIRCLE('',#9198,0.32);
#3682=CIRCLE('',#9200,0.22);
#3683=CIRCLE('',#9202,0.1954);
#3684=CIRCLE('',#9204,0.1954);
#3685=CIRCLE('',#9206,0.16);
#4220=VERTEX_POINT('',#13662);
#4221=VERTEX_POINT('',#13665);
#4222=VERTEX_POINT('',#13669);
#4223=VERTEX_POINT('',#13673);
#4224=VERTEX_POINT('',#13677);
#4225=VERTEX_POINT('',#13680);
#4226=VERTEX_POINT('',#13684);
#4227=VERTEX_POINT('',#13688);
#4228=VERTEX_POINT('',#13693);
#4229=VERTEX_POINT('',#13694);
#4230=VERTEX_POINT('',#13696);
#4231=VERTEX_POINT('',#13698);
#4232=VERTEX_POINT('',#13702);
#4233=VERTEX_POINT('',#13704);
#4234=VERTEX_POINT('',#13708);
#4235=VERTEX_POINT('',#13710);
#4236=VERTEX_POINT('',#13714);
#4237=VERTEX_POINT('',#13716);
#4238=VERTEX_POINT('',#13720);
#4239=VERTEX_POINT('',#13722);
#5107=EDGE_CURVE('',#4220,#4220,#3678,.T.);
#5108=EDGE_CURVE('',#4221,#4221,#3679,.T.);
#5109=EDGE_CURVE('',#4221,#4220,#2693,.T.);
#5110=EDGE_CURVE('',#4222,#4222,#3680,.T.);
#5111=EDGE_CURVE('',#4222,#4221,#2694,.T.);
#5112=EDGE_CURVE('',#4223,#4223,#3681,.T.);
#5113=EDGE_CURVE('',#4223,#4222,#2695,.T.);
#5114=EDGE_CURVE('',#4224,#4224,#3682,.T.);
#5115=EDGE_CURVE('',#4225,#4225,#3683,.F.);
#5116=EDGE_CURVE('',#4225,#4224,#2696,.T.);
#5117=EDGE_CURVE('',#4226,#4226,#3684,.F.);
#5118=EDGE_CURVE('',#4226,#4225,#2697,.T.);
#5119=EDGE_CURVE('',#4227,#4227,#3685,.T.);
#5120=EDGE_CURVE('',#4227,#4226,#2698,.T.);
#5121=EDGE_CURVE('',#4228,#4229,#2699,.T.);
#5122=EDGE_CURVE('',#4229,#4230,#2700,.T.);
#5123=EDGE_CURVE('',#4230,#4231,#2701,.T.);
#5124=EDGE_CURVE('',#4228,#4231,#2702,.T.);
#5125=EDGE_CURVE('',#4229,#4232,#2703,.T.);
#5126=EDGE_CURVE('',#4232,#4233,#2704,.T.);
#5127=EDGE_CURVE('',#4233,#4230,#2705,.T.);
#5128=EDGE_CURVE('',#4232,#4234,#2706,.T.);
#5129=EDGE_CURVE('',#4234,#4235,#2707,.T.);
#5130=EDGE_CURVE('',#4235,#4233,#2708,.T.);
#5131=EDGE_CURVE('',#4234,#4236,#2709,.T.);
#5132=EDGE_CURVE('',#4236,#4237,#2710,.T.);
#5133=EDGE_CURVE('',#4237,#4235,#2711,.T.);
#5134=EDGE_CURVE('',#4236,#4238,#2712,.T.);
#5135=EDGE_CURVE('',#4238,#4239,#2713,.T.);
#5136=EDGE_CURVE('',#4239,#4237,#2714,.T.);
#5137=EDGE_CURVE('',#4238,#4228,#2715,.T.);
#5138=EDGE_CURVE('',#4231,#4239,#2716,.T.);
#6818=ORIENTED_EDGE('',*,*,#5107,.F.);
#6819=ORIENTED_EDGE('',*,*,#5108,.F.);
#6820=ORIENTED_EDGE('',*,*,#5109,.T.);
#6821=ORIENTED_EDGE('',*,*,#5107,.T.);
#6822=ORIENTED_EDGE('',*,*,#5109,.F.);
#6823=ORIENTED_EDGE('',*,*,#5110,.F.);
#6824=ORIENTED_EDGE('',*,*,#5111,.T.);
#6825=ORIENTED_EDGE('',*,*,#5108,.T.);
#6826=ORIENTED_EDGE('',*,*,#5111,.F.);
#6827=ORIENTED_EDGE('',*,*,#5112,.F.);
#6828=ORIENTED_EDGE('',*,*,#5113,.T.);
#6829=ORIENTED_EDGE('',*,*,#5110,.T.);
#6830=ORIENTED_EDGE('',*,*,#5113,.F.);
#6831=ORIENTED_EDGE('',*,*,#5112,.T.);
#6832=ORIENTED_EDGE('',*,*,#5114,.F.);
#6833=ORIENTED_EDGE('',*,*,#5115,.F.);
#6834=ORIENTED_EDGE('',*,*,#5116,.T.);
#6835=ORIENTED_EDGE('',*,*,#5114,.T.);
#6836=ORIENTED_EDGE('',*,*,#5116,.F.);
#6837=ORIENTED_EDGE('',*,*,#5117,.F.);
#6838=ORIENTED_EDGE('',*,*,#5118,.T.);
#6839=ORIENTED_EDGE('',*,*,#5115,.T.);
#6840=ORIENTED_EDGE('',*,*,#5118,.F.);
#6841=ORIENTED_EDGE('',*,*,#5119,.F.);
#6842=ORIENTED_EDGE('',*,*,#5120,.T.);
#6843=ORIENTED_EDGE('',*,*,#5117,.T.);
#6844=ORIENTED_EDGE('',*,*,#5120,.F.);
#6845=ORIENTED_EDGE('',*,*,#5119,.T.);
#6846=ORIENTED_EDGE('',*,*,#5121,.T.);
#6847=ORIENTED_EDGE('',*,*,#5122,.T.);
#6848=ORIENTED_EDGE('',*,*,#5123,.T.);
#6849=ORIENTED_EDGE('',*,*,#5124,.F.);
#6850=ORIENTED_EDGE('',*,*,#5125,.T.);
#6851=ORIENTED_EDGE('',*,*,#5126,.T.);
#6852=ORIENTED_EDGE('',*,*,#5127,.T.);
#6853=ORIENTED_EDGE('',*,*,#5122,.F.);
#6854=ORIENTED_EDGE('',*,*,#5128,.T.);
#6855=ORIENTED_EDGE('',*,*,#5129,.T.);
#6856=ORIENTED_EDGE('',*,*,#5130,.T.);
#6857=ORIENTED_EDGE('',*,*,#5126,.F.);
#6858=ORIENTED_EDGE('',*,*,#5131,.T.);
#6859=ORIENTED_EDGE('',*,*,#5132,.T.);
#6860=ORIENTED_EDGE('',*,*,#5133,.T.);
#6861=ORIENTED_EDGE('',*,*,#5129,.F.);
#6862=ORIENTED_EDGE('',*,*,#5134,.T.);
#6863=ORIENTED_EDGE('',*,*,#5135,.T.);
#6864=ORIENTED_EDGE('',*,*,#5136,.T.);
#6865=ORIENTED_EDGE('',*,*,#5132,.F.);
#6866=ORIENTED_EDGE('',*,*,#5137,.T.);
#6867=ORIENTED_EDGE('',*,*,#5124,.T.);
#6868=ORIENTED_EDGE('',*,*,#5138,.T.);
#6869=ORIENTED_EDGE('',*,*,#5135,.F.);
#6870=ORIENTED_EDGE('',*,*,#5137,.F.);
#6871=ORIENTED_EDGE('',*,*,#5134,.F.);
#6872=ORIENTED_EDGE('',*,*,#5131,.F.);
#6873=ORIENTED_EDGE('',*,*,#5128,.F.);
#6874=ORIENTED_EDGE('',*,*,#5125,.F.);
#6875=ORIENTED_EDGE('',*,*,#5121,.F.);
#6876=ORIENTED_EDGE('',*,*,#5138,.F.);
#6877=ORIENTED_EDGE('',*,*,#5123,.F.);
#6878=ORIENTED_EDGE('',*,*,#5127,.F.);
#6879=ORIENTED_EDGE('',*,*,#5130,.F.);
#6880=ORIENTED_EDGE('',*,*,#5133,.F.);
#6881=ORIENTED_EDGE('',*,*,#5136,.F.);
#7377=CYLINDRICAL_SURFACE('',#9195,0.35);
#7378=CYLINDRICAL_SURFACE('',#9203,0.1954);
#7774=ADVANCED_FACE('',(#1492),#1051,.T.);
#7775=ADVANCED_FACE('',(#1493),#441,.T.);
#7776=ADVANCED_FACE('',(#1494),#7377,.T.);
#7777=ADVANCED_FACE('',(#1495),#442,.T.);
#7778=ADVANCED_FACE('',(#1496,#797),#1052,.T.);
#7779=ADVANCED_FACE('',(#1497),#443,.T.);
#7780=ADVANCED_FACE('',(#1498),#7378,.T.);
#7781=ADVANCED_FACE('',(#1499),#444,.T.);
#7782=ADVANCED_FACE('',(#1500),#1053,.T.);
#7783=ADVANCED_FACE('',(#1501),#1054,.F.);
#7784=ADVANCED_FACE('',(#1502),#1055,.F.);
#7785=ADVANCED_FACE('',(#1503),#1056,.F.);
#7786=ADVANCED_FACE('',(#1504),#1057,.F.);
#7787=ADVANCED_FACE('',(#1505),#1058,.F.);
#7788=ADVANCED_FACE('',(#1506),#1059,.F.);
#7789=ADVANCED_FACE('',(#1507),#1060,.F.);
#7790=ADVANCED_FACE('',(#1508),#1061,.F.);
#7909=CLOSED_SHELL('',(#7774,#7775,#7776,#7777,#7778,#7779,#7780,#7781,
#7782));
#7910=CLOSED_SHELL('',(#7783,#7784,#7785,#7786,#7787,#7788,#7789,#7790));
#9190=AXIS2_PLACEMENT_3D('',#13660,#11408,#11409);
#9191=AXIS2_PLACEMENT_3D('',#13661,#11410,#11411);
#9192=AXIS2_PLACEMENT_3D('',#13663,#11412,#11413);
#9193=AXIS2_PLACEMENT_3D('',#13664,#11414,#11415);
#9194=AXIS2_PLACEMENT_3D('',#13666,#11416,#11417);
#9195=AXIS2_PLACEMENT_3D('',#13668,#11419,#11420);
#9196=AXIS2_PLACEMENT_3D('',#13670,#11421,#11422);
#9197=AXIS2_PLACEMENT_3D('',#13672,#11424,#11425);
#9198=AXIS2_PLACEMENT_3D('',#13674,#11426,#11427);
#9199=AXIS2_PLACEMENT_3D('',#13676,#11429,#11430);
#9200=AXIS2_PLACEMENT_3D('',#13678,#11431,#11432);
#9201=AXIS2_PLACEMENT_3D('',#13679,#11433,#11434);
#9202=AXIS2_PLACEMENT_3D('',#13681,#11435,#11436);
#9203=AXIS2_PLACEMENT_3D('',#13683,#11438,#11439);
#9204=AXIS2_PLACEMENT_3D('',#13685,#11440,#11441);
#9205=AXIS2_PLACEMENT_3D('',#13687,#11443,#11444);
#9206=AXIS2_PLACEMENT_3D('',#13689,#11445,#11446);
#9207=AXIS2_PLACEMENT_3D('',#13691,#11448,#11449);
#9208=AXIS2_PLACEMENT_3D('',#13692,#11450,#11451);
#9209=AXIS2_PLACEMENT_3D('',#13701,#11456,#11457);
#9210=AXIS2_PLACEMENT_3D('',#13707,#11461,#11462);
#9211=AXIS2_PLACEMENT_3D('',#13713,#11466,#11467);
#9212=AXIS2_PLACEMENT_3D('',#13719,#11471,#11472);
#9213=AXIS2_PLACEMENT_3D('',#13725,#11476,#11477);
#9214=AXIS2_PLACEMENT_3D('',#13728,#11480,#11481);
#9215=AXIS2_PLACEMENT_3D('',#13729,#11482,#11483);
#11408=DIRECTION('axis',(0.,0.,1.));
#11409=DIRECTION('refdir',(1.,0.,0.));
#11410=DIRECTION('center_axis',(0.,1.,0.));
#11411=DIRECTION('ref_axis',(0.,0.,1.));
#11412=DIRECTION('center_axis',(0.,-1.,0.));
#11413=DIRECTION('ref_axis',(1.,0.,0.));
#11414=DIRECTION('center_axis',(0.,-1.,0.));
#11415=DIRECTION('ref_axis',(1.,0.,0.));
#11416=DIRECTION('center_axis',(0.,-1.,0.));
#11417=DIRECTION('ref_axis',(1.,0.,0.));
#11418=DIRECTION('',(0.707106781186547,0.707106781186548,8.65956056235493E-17));
#11419=DIRECTION('center_axis',(0.,-1.,0.));
#11420=DIRECTION('ref_axis',(1.,0.,0.));
#11421=DIRECTION('center_axis',(0.,-1.,0.));
#11422=DIRECTION('ref_axis',(1.,0.,0.));
#11423=DIRECTION('',(0.,1.,0.));
#11424=DIRECTION('center_axis',(0.,1.,0.));
#11425=DIRECTION('ref_axis',(1.,0.,0.));
#11426=DIRECTION('center_axis',(0.,-1.,0.));
#11427=DIRECTION('ref_axis',(1.,0.,0.));
#11428=DIRECTION('',(-0.707106781186547,0.707106781186548,-8.65956056235493E-17));
#11429=DIRECTION('center_axis',(0.,-1.,0.));
#11430=DIRECTION('ref_axis',(0.,0.,-1.));
#11431=DIRECTION('center_axis',(0.,-1.,0.));
#11432=DIRECTION('ref_axis',(1.,0.,0.));
#11433=DIRECTION('center_axis',(0.,1.,0.));
#11434=DIRECTION('ref_axis',(1.,0.,0.));
#11435=DIRECTION('center_axis',(0.,1.,0.));
#11436=DIRECTION('ref_axis',(1.,0.,0.));
#11437=DIRECTION('',(-0.447213595499958,0.894427190999916,-5.47678698264203E-17));
#11438=DIRECTION('center_axis',(0.,-1.,0.));
#11439=DIRECTION('ref_axis',(1.,0.,0.));
#11440=DIRECTION('center_axis',(0.,1.,0.));
#11441=DIRECTION('ref_axis',(1.,0.,0.));
#11442=DIRECTION('',(0.,1.,0.));
#11443=DIRECTION('center_axis',(0.,1.,0.));
#11444=DIRECTION('ref_axis',(1.,0.,0.));
#11445=DIRECTION('center_axis',(0.,-1.,0.));
#11446=DIRECTION('ref_axis',(1.,0.,0.));
#11447=DIRECTION('',(-0.707106781186547,0.707106781186548,-8.65956056235493E-17));
#11448=DIRECTION('center_axis',(0.,-1.,0.));
#11449=DIRECTION('ref_axis',(0.,0.,-1.));
#11450=DIRECTION('center_axis',(0.866025403784439,0.,-0.5));
#11451=DIRECTION('ref_axis',(0.5,0.,0.866025403784439));
#11452=DIRECTION('',(-0.5,0.,-0.866025403784439));
#11453=DIRECTION('',(0.,-1.,0.));
#11454=DIRECTION('',(0.5,0.,0.866025403784439));
#11455=DIRECTION('',(0.,-1.,0.));
#11456=DIRECTION('center_axis',(1.60246890531964E-16,0.,-1.));
#11457=DIRECTION('ref_axis',(1.,0.,1.60246890531964E-16));
#11458=DIRECTION('',(-1.,0.,-1.60246890531964E-16));
#11459=DIRECTION('',(0.,-1.,0.));
#11460=DIRECTION('',(1.,0.,1.60246890531964E-16));
#11461=DIRECTION('center_axis',(-0.866025403784439,0.,-0.5));
#11462=DIRECTION('ref_axis',(0.5,0.,-0.866025403784439));
#11463=DIRECTION('',(-0.5,0.,0.866025403784439));
#11464=DIRECTION('',(0.,-1.,0.));
#11465=DIRECTION('',(0.5,0.,-0.866025403784439));
#11466=DIRECTION('center_axis',(-0.866025403784439,0.,0.5));
#11467=DIRECTION('ref_axis',(-0.5,0.,-0.866025403784439));
#11468=DIRECTION('',(0.5,0.,0.866025403784439));
#11469=DIRECTION('',(0.,-1.,0.));
#11470=DIRECTION('',(-0.5,0.,-0.866025403784439));
#11471=DIRECTION('center_axis',(-1.60246890531964E-16,0.,1.));
#11472=DIRECTION('ref_axis',(-1.,0.,-1.60246890531964E-16));
#11473=DIRECTION('',(1.,0.,1.60246890531964E-16));
#11474=DIRECTION('',(0.,-1.,0.));
#11475=DIRECTION('',(-1.,0.,-1.60246890531964E-16));
#11476=DIRECTION('center_axis',(0.866025403784439,0.,0.5));
#11477=DIRECTION('ref_axis',(-0.5,0.,0.866025403784439));
#11478=DIRECTION('',(0.5,0.,-0.866025403784439));
#11479=DIRECTION('',(-0.5,0.,0.866025403784439));
#11480=DIRECTION('center_axis',(0.,1.,0.));
#11481=DIRECTION('ref_axis',(1.,0.,0.));
#11482=DIRECTION('center_axis',(0.,-1.,0.));
#11483=DIRECTION('ref_axis',(0.,0.,-1.));
#13660=CARTESIAN_POINT('',(0.,0.,0.));
#13661=CARTESIAN_POINT('Origin',(0.3,0.4,0.));
#13662=CARTESIAN_POINT('',(-0.3,0.4,-3.67394039744206E-17));
#13663=CARTESIAN_POINT('Origin',(0.,0.4,0.));
#13664=CARTESIAN_POINT('Origin',(0.,0.375,0.));
#13665=CARTESIAN_POINT('',(-0.35,0.35,-4.28626379701573E-17));
#13666=CARTESIAN_POINT('Origin',(0.,0.35,0.));
#13667=CARTESIAN_POINT('',(-0.325,0.375,-3.9801020972289E-17));
#13668=CARTESIAN_POINT('Origin',(0.,0.19,0.));
#13669=CARTESIAN_POINT('',(-0.35,0.03,-4.28626379701574E-17));
#13670=CARTESIAN_POINT('Origin',(0.,0.03,0.));
#13671=CARTESIAN_POINT('',(-0.35,0.19,-4.28626379701574E-17));
#13672=CARTESIAN_POINT('Origin',(0.,0.0149999999999999,0.));
#13673=CARTESIAN_POINT('',(-0.32,-3.29597460435593E-17,-3.91886975727153E-17));
#13674=CARTESIAN_POINT('Origin',(0.,0.,0.));
#13675=CARTESIAN_POINT('',(-0.335,0.0149999999999999,-4.10256677714363E-17));
#13676=CARTESIAN_POINT('Origin',(0.22,0.,0.));
#13677=CARTESIAN_POINT('',(-0.22,-6.93889390390723E-18,-2.69422295812418E-17));
#13678=CARTESIAN_POINT('Origin',(0.,0.,0.));
#13679=CARTESIAN_POINT('Origin',(0.,-0.02,0.));
#13680=CARTESIAN_POINT('',(-0.1954,-0.0492,2.39295984553393E-17));
#13681=CARTESIAN_POINT('Origin',(0.,-0.0492,0.));
#13682=CARTESIAN_POINT('',(-0.21,-0.02,-2.57175827820944E-17));
#13683=CARTESIAN_POINT('Origin',(0.,-0.8,0.));
#13684=CARTESIAN_POINT('',(-0.1954,-1.5646,2.39295984553393E-17));
#13685=CARTESIAN_POINT('Origin',(0.,-1.5646,0.));
#13686=CARTESIAN_POINT('',(-0.1954,-0.8,-2.39295984553393E-17));
#13687=CARTESIAN_POINT('Origin',(0.,-1.58,0.));
#13688=CARTESIAN_POINT('',(-0.16,-1.6,-1.95943487863577E-17));
#13689=CARTESIAN_POINT('Origin',(0.,-1.6,0.));
#13690=CARTESIAN_POINT('',(-0.18,-1.58,-2.20436423846524E-17));
#13691=CARTESIAN_POINT('Origin',(0.,-1.6,0.));
#13692=CARTESIAN_POINT('Origin',(0.0866025403784439,-0.4,-0.15));
#13693=CARTESIAN_POINT('',(0.173205080756888,-0.4,0.));
#13694=CARTESIAN_POINT('',(0.0866025403784439,-0.4,-0.15));
#13695=CARTESIAN_POINT('',(0.173205080756888,-0.4,0.));
#13696=CARTESIAN_POINT('',(0.0866025403784439,-0.64,-0.15));
#13697=CARTESIAN_POINT('',(0.0866025403784439,-0.4,-0.15));
#13698=CARTESIAN_POINT('',(0.173205080756888,-0.64,0.));
#13699=CARTESIAN_POINT('',(0.173205080756888,-0.64,0.));
#13700=CARTESIAN_POINT('',(0.173205080756888,-0.4,0.));
#13701=CARTESIAN_POINT('Origin',(-0.0866025403784438,-0.4,-0.15));
#13702=CARTESIAN_POINT('',(-0.0866025403784438,-0.4,-0.15));
#13703=CARTESIAN_POINT('',(0.0866025403784439,-0.4,-0.15));
#13704=CARTESIAN_POINT('',(-0.0866025403784438,-0.64,-0.15));
#13705=CARTESIAN_POINT('',(-0.0866025403784438,-0.4,-0.15));
#13706=CARTESIAN_POINT('',(0.0866025403784439,-0.64,-0.15));
#13707=CARTESIAN_POINT('Origin',(-0.173205080756888,-0.4,-2.77555756156289E-17));
#13708=CARTESIAN_POINT('',(-0.173205080756888,-0.4,-2.12115047744981E-17));
#13709=CARTESIAN_POINT('',(-0.0866025403784438,-0.4,-0.15));
#13710=CARTESIAN_POINT('',(-0.173205080756888,-0.64,-2.77555756156289E-17));
#13711=CARTESIAN_POINT('',(-0.173205080756888,-0.4,-2.12115047744981E-17));
#13712=CARTESIAN_POINT('',(-0.0866025403784438,-0.64,-0.15));
#13713=CARTESIAN_POINT('Origin',(-0.0866025403784439,-0.4,0.15));
#13714=CARTESIAN_POINT('',(-0.0866025403784439,-0.4,0.15));
#13715=CARTESIAN_POINT('',(-0.173205080756888,-0.4,-2.12115047744981E-17));
#13716=CARTESIAN_POINT('',(-0.0866025403784439,-0.64,0.15));
#13717=CARTESIAN_POINT('',(-0.0866025403784439,-0.4,0.15));
#13718=CARTESIAN_POINT('',(-0.173205080756888,-0.64,-2.12115047744981E-17));
#13719=CARTESIAN_POINT('Origin',(0.0866025403784439,-0.4,0.15));
#13720=CARTESIAN_POINT('',(0.0866025403784439,-0.4,0.15));
#13721=CARTESIAN_POINT('',(-0.0866025403784439,-0.4,0.15));
#13722=CARTESIAN_POINT('',(0.0866025403784439,-0.64,0.15));
#13723=CARTESIAN_POINT('',(0.0866025403784439,-0.4,0.15));
#13724=CARTESIAN_POINT('',(-0.0866025403784439,-0.64,0.15));
#13725=CARTESIAN_POINT('Origin',(0.173205080756888,-0.4,0.));
#13726=CARTESIAN_POINT('',(0.0866025403784439,-0.4,0.15));
#13727=CARTESIAN_POINT('',(0.0866025403784439,-0.64,0.15));
#13728=CARTESIAN_POINT('Origin',(0.,-0.4,-2.77555756156289E-17));
#13729=CARTESIAN_POINT('Origin',(0.,-0.64,-2.77555756156289E-17));
#14333=UNCERTAINTY_MEASURE_WITH_UNIT(LENGTH_MEASURE(0.001),#14393,
'DISTANCE_ACCURACY_VALUE',
'Maximum model space distance between geometric entities at asserted c
onnectivities');
#14344=UNCERTAINTY_MEASURE_WITH_UNIT(LENGTH_MEASURE(0.001),#14393,
'DISTANCE_ACCURACY_VALUE',
'Maximum model space distance between geometric entities at asserted c
onnectivities');
#14381=(
GEOMETRIC_REPRESENTATION_CONTEXT(3)
GLOBAL_UNCERTAINTY_ASSIGNED_CONTEXT((#14333))
GLOBAL_UNIT_ASSIGNED_CONTEXT((#14393,#14395,#14396))
REPRESENTATION_CONTEXT('','3D')
);
#14392=(
GEOMETRIC_REPRESENTATION_CONTEXT(3)
GLOBAL_UNCERTAINTY_ASSIGNED_CONTEXT((#14344))
GLOBAL_UNIT_ASSIGNED_CONTEXT((#14393,#14395,#14396))
REPRESENTATION_CONTEXT('','3D')
);
#14393=(
LENGTH_UNIT()
NAMED_UNIT(*)
SI_UNIT(.CENTI.,.METRE.)
);
#14395=(
NAMED_UNIT(*)
PLANE_ANGLE_UNIT()
SI_UNIT($,.RADIAN.)
);
#14396=(
NAMED_UNIT(*)
SI_UNIT($,.STERADIAN.)
SOLID_ANGLE_UNIT()
);
#14433=SHAPE_DEFINITION_REPRESENTATION(#14552,#14619);
#14552=PRODUCT_DEFINITION_SHAPE('',$,#14667);
#14619=SHAPE_REPRESENTATION('',(#9190),#14381);
#14630=PRODUCT_DEFINITION_CONTEXT('part definition',#14773,'design');
#14667=PRODUCT_DEFINITION('Cap Screw - M4x16','Cap Screw - M4x16',#14714,
#14630);
#14714=PRODUCT_DEFINITION_FORMATION('',$,#14811);
#14773=APPLICATION_CONTEXT(
'Core Data for Automotive Mechanical Design Process');
#14774=PRODUCT_CONTEXT('part definition',#14773,'mechanical');
#14811=PRODUCT('Cap Screw - M4x16','Cap Screw - M4x16',
'Cap Screw - M4x16',(#14774));
#14892=COLOUR_RGB('Black',0.12,0.14,0.17);
#14893=FILL_AREA_STYLE_COLOUR('',#14892);
#14894=FILL_AREA_STYLE('',(#14893));
#14895=SURFACE_STYLE_FILL_AREA(#14894);
#14896=SURFACE_SIDE_STYLE('',(#14895));
#14897=SURFACE_STYLE_USAGE(.BOTH.,#14896);
#14898=PRESENTATION_STYLE_ASSIGNMENT((#14897));
ENDSEC;
END-ISO-10303-21;
